ISO-10303-21;
HEADER;
/* Generated by software containing ST-Developer
 * from STEP Tools, Inc. (www.steptools.com) 
 */

FILE_DESCRIPTION(
/* description */ (''),
/* implementation_level */ '2;1');

FILE_NAME(
/* name */ 'Nut_01.step',
/* time_stamp */ '2026-10-06T13:05:37-07:00',
/* author */ (''),
/* organization */ (''),
/* preprocessor_version */ 'ST-DEVELOPER v20.2',
/* originating_system */ 'Autodesk Translation Framework v15.15.0.0',
/* authorisation */ '');

FILE_SCHEMA (('AUTOMOTIVE_DESIGN { 1 0 10303 214 3 1 1 }'));
ENDSEC;

DATA;
#10=MECHANICAL_DESIGN_GEOMETRIC_PRESENTATION_REPRESENTATION('',(#144),#28055);
#94=B_SPLINE_SURFACE_WITH_KNOTS('',3,1,((#25707,#25708),(#25709,#25710),
(#25711,#25712),(#25713,#25714),(#25715,#25716),(#25717,#25718),(#25719,
#25720),(#25721,#25722),(#25723,#25724),(#25725,#25726),(#25727,#25728),
(#25729,#25730),(#25731,#25732),(#25733,#25734)),.UNSPECIFIED.,.F.,.F.,
 .F.,(4,2,2,2,2,2,4),(2,2),(-0.844212290556731,-0.730966332817565,-0.619975754240938,
-0.457326579004558,-0.29977928179387,-0.147336283383114,0.),(0.,0.48),
 .UNSPECIFIED.);
#95=B_SPLINE_SURFACE_WITH_KNOTS('',3,1,((#25775,#25776),(#25777,#25778),
(#25779,#25780),(#25781,#25782),(#25783,#25784),(#25785,#25786),(#25787,
#25788),(#25789,#25790),(#25791,#25792),(#25793,#25794),(#25795,#25796),
(#25797,#25798),(#25799,#25800),(#25801,#25802)),.UNSPECIFIED.,.F.,.F.,
 .F.,(4,2,2,2,2,2,4),(2,2),(-0.847325527525843,-0.749719327139836,-0.649860858750851,
-0.495073659399383,-0.335166304629316,-0.170141007879843,0.),(0.,0.48),
 .UNSPECIFIED.);
#124=SHAPE_REPRESENTATION_RELATIONSHIP('SRR','None',#28101,#134);
#134=ADVANCED_BREP_SHAPE_REPRESENTATION('',(#153),#28053);
#144=STYLED_ITEM('',(#28152),#153);
#153=MANIFOLD_SOLID_BREP('Body1',#3687);
#201=FACE_BOUND('',#814,.T.);
#202=FACE_BOUND('',#816,.T.);
#246=PLANE('',#4093);
#247=PLANE('',#4094);
#248=PLANE('',#4095);
#249=PLANE('',#4096);
#250=PLANE('',#4097);
#251=PLANE('',#4098);
#252=PLANE('',#4099);
#253=PLANE('',#4100);
#375=CIRCLE('',#4088,4.433);
#376=CIRCLE('',#4089,4.433);
#377=CIRCLE('',#4091,3.72275);
#378=CIRCLE('',#4092,3.72275);
#569=FACE_OUTER_BOUND('',#803,.T.);
#570=FACE_OUTER_BOUND('',#804,.T.);
#571=FACE_OUTER_BOUND('',#805,.T.);
#572=FACE_OUTER_BOUND('',#806,.T.);
#573=FACE_OUTER_BOUND('',#807,.T.);
#574=FACE_OUTER_BOUND('',#808,.T.);
#575=FACE_OUTER_BOUND('',#809,.T.);
#576=FACE_OUTER_BOUND('',#810,.T.);
#577=FACE_OUTER_BOUND('',#811,.T.);
#578=FACE_OUTER_BOUND('',#812,.T.);
#579=FACE_OUTER_BOUND('',#813,.T.);
#580=FACE_OUTER_BOUND('',#815,.T.);
#803=EDGE_LOOP('',(#3322,#3323,#3324,#3325));
#804=EDGE_LOOP('',(#3326,#3327,#3328,#3329));
#805=EDGE_LOOP('',(#3330,#3331,#3332,#3333));
#806=EDGE_LOOP('',(#3334,#3335,#3336,#3337));
#807=EDGE_LOOP('',(#3338,#3339,#3340,#3341));
#808=EDGE_LOOP('',(#3342,#3343,#3344,#3345));
#809=EDGE_LOOP('',(#3346,#3347,#3348,#3349));
#810=EDGE_LOOP('',(#3350,#3351,#3352,#3353));
#811=EDGE_LOOP('',(#3354,#3355,#3356,#3357));
#812=EDGE_LOOP('',(#3358,#3359,#3360,#3361));
#813=EDGE_LOOP('',(#3362,#3363,#3364,#3365,#3366,#3367));
#814=EDGE_LOOP('',(#3368,#3369,#3370,#3371));
#815=EDGE_LOOP('',(#3372,#3373,#3374,#3375,#3376,#3377));
#816=EDGE_LOOP('',(#3378,#3379,#3380,#3381));
#957=LINE('',#25752,#1115);
#958=LINE('',#25768,#1116);
#959=LINE('',#25774,#1117);
#960=LINE('',#25833,#1118);
#961=LINE('',#25840,#1119);
#962=LINE('',#25842,#1120);
#963=LINE('',#25844,#1121);
#964=LINE('',#25845,#1122);
#965=LINE('',#25848,#1123);
#966=LINE('',#25850,#1124);
#967=LINE('',#25851,#1125);
#968=LINE('',#25854,#1126);
#969=LINE('',#25856,#1127);
#970=LINE('',#25857,#1128);
#971=LINE('',#25860,#1129);
#972=LINE('',#25862,#1130);
#973=LINE('',#25863,#1131);
#974=LINE('',#25866,#1132);
#975=LINE('',#25868,#1133);
#976=LINE('',#25869,#1134);
#977=LINE('',#25871,#1135);
#978=LINE('',#25872,#1136);
#1115=VECTOR('',#4824,10.);
#1116=VECTOR('',#4825,10.);
#1117=VECTOR('',#4832,10.);
#1118=VECTOR('',#4833,10.);
#1119=VECTOR('',#4842,10.);
#1120=VECTOR('',#4843,10.);
#1121=VECTOR('',#4844,10.);
#1122=VECTOR('',#4845,10.);
#1123=VECTOR('',#4848,9.99999999999999);
#1124=VECTOR('',#4849,9.99999999999999);
#1125=VECTOR('',#4850,10.);
#1126=VECTOR('',#4853,10.);
#1127=VECTOR('',#4854,10.);
#1128=VECTOR('',#4855,10.);
#1129=VECTOR('',#4858,10.);
#1130=VECTOR('',#4859,10.);
#1131=VECTOR('',#4860,10.);
#1132=VECTOR('',#4863,10.);
#1133=VECTOR('',#4864,10.);
#1134=VECTOR('',#4865,10.);
#1135=VECTOR('',#4868,10.);
#1136=VECTOR('',#4869,10.);
#1384=B_SPLINE_CURVE_WITH_KNOTS('',3,(#25737,#25738,#25739,#25740,#25741,
#25742,#25743,#25744,#25745,#25746,#25747,#25748,#25749,#25750),
 .UNSPECIFIED.,.F.,.F.,(4,2,2,2,2,2,4),(-0.844212290556731,-0.730966332817565,
-0.619975754240938,-0.457326579004558,-0.29977928179387,-0.147336283383114,
0.),.UNSPECIFIED.);
#1385=B_SPLINE_CURVE_WITH_KNOTS('',3,(#25754,#25755,#25756,#25757,#25758,
#25759,#25760,#25761,#25762,#25763,#25764,#25765,#25766,#25767),
 .UNSPECIFIED.,.F.,.F.,(4,2,2,2,2,2,4),(-0.844212290556731,-0.730966332817565,
-0.619975754240938,-0.457326579004558,-0.29977928179387,-0.147336283383114,
0.),.UNSPECIFIED.);
#1386=B_SPLINE_CURVE_WITH_KNOTS('',3,(#25804,#25805,#25806,#25807,#25808,
#25809,#25810,#25811,#25812,#25813,#25814,#25815,#25816,#25817),
 .UNSPECIFIED.,.F.,.F.,(4,2,2,2,2,2,4),(-0.847325527525843,-0.749719327139836,
-0.649860858750851,-0.495073659399383,-0.335166304629316,-0.170141007879843,
0.),.UNSPECIFIED.);
#1387=B_SPLINE_CURVE_WITH_KNOTS('',3,(#25819,#25820,#25821,#25822,#25823,
#25824,#25825,#25826,#25827,#25828,#25829,#25830,#25831,#25832),
 .UNSPECIFIED.,.F.,.F.,(4,2,2,2,2,2,4),(-0.847325527525843,-0.749719327139836,
-0.649860858750851,-0.495073659399383,-0.335166304629316,-0.170141007879843,
0.),.UNSPECIFIED.);
#1744=VERTEX_POINT('',#25735);
#1745=VERTEX_POINT('',#25736);
#1746=VERTEX_POINT('',#25751);
#1747=VERTEX_POINT('',#25753);
#1748=VERTEX_POINT('',#25770);
#1749=VERTEX_POINT('',#25772);
#1750=VERTEX_POINT('',#25803);
#1751=VERTEX_POINT('',#25818);
#1752=VERTEX_POINT('',#25838);
#1753=VERTEX_POINT('',#25839);
#1754=VERTEX_POINT('',#25841);
#1755=VERTEX_POINT('',#25843);
#1756=VERTEX_POINT('',#25847);
#1757=VERTEX_POINT('',#25849);
#1758=VERTEX_POINT('',#25853);
#1759=VERTEX_POINT('',#25855);
#1760=VERTEX_POINT('',#25859);
#1761=VERTEX_POINT('',#25861);
#1762=VERTEX_POINT('',#25865);
#1763=VERTEX_POINT('',#25867);
#2274=EDGE_CURVE('',#1744,#1745,#1384,.T.);
#2275=EDGE_CURVE('',#1745,#1746,#957,.T.);
#2276=EDGE_CURVE('',#1747,#1746,#1385,.T.);
#2277=EDGE_CURVE('',#1744,#1747,#958,.T.);
#2278=EDGE_CURVE('',#1748,#1744,#375,.T.);
#2279=EDGE_CURVE('',#1749,#1747,#376,.T.);
#2280=EDGE_CURVE('',#1748,#1749,#959,.T.);
#2281=EDGE_CURVE('',#1750,#1748,#1386,.T.);
#2282=EDGE_CURVE('',#1751,#1749,#1387,.T.);
#2283=EDGE_CURVE('',#1750,#1751,#960,.T.);
#2284=EDGE_CURVE('',#1745,#1750,#377,.T.);
#2285=EDGE_CURVE('',#1746,#1751,#378,.T.);
#2286=EDGE_CURVE('',#1752,#1753,#961,.T.);
#2287=EDGE_CURVE('',#1753,#1754,#962,.T.);
#2288=EDGE_CURVE('',#1755,#1754,#963,.T.);
#2289=EDGE_CURVE('',#1752,#1755,#964,.T.);
#2290=EDGE_CURVE('',#1756,#1752,#965,.T.);
#2291=EDGE_CURVE('',#1757,#1755,#966,.T.);
#2292=EDGE_CURVE('',#1756,#1757,#967,.T.);
#2293=EDGE_CURVE('',#1758,#1756,#968,.T.);
#2294=EDGE_CURVE('',#1759,#1757,#969,.T.);
#2295=EDGE_CURVE('',#1758,#1759,#970,.T.);
#2296=EDGE_CURVE('',#1760,#1758,#971,.T.);
#2297=EDGE_CURVE('',#1761,#1759,#972,.T.);
#2298=EDGE_CURVE('',#1760,#1761,#973,.T.);
#2299=EDGE_CURVE('',#1762,#1760,#974,.T.);
#2300=EDGE_CURVE('',#1763,#1761,#975,.T.);
#2301=EDGE_CURVE('',#1762,#1763,#976,.T.);
#2302=EDGE_CURVE('',#1753,#1762,#977,.T.);
#2303=EDGE_CURVE('',#1754,#1763,#978,.T.);
#3322=ORIENTED_EDGE('',*,*,#2274,.T.);
#3323=ORIENTED_EDGE('',*,*,#2275,.T.);
#3324=ORIENTED_EDGE('',*,*,#2276,.F.);
#3325=ORIENTED_EDGE('',*,*,#2277,.F.);
#3326=ORIENTED_EDGE('',*,*,#2278,.T.);
#3327=ORIENTED_EDGE('',*,*,#2277,.T.);
#3328=ORIENTED_EDGE('',*,*,#2279,.F.);
#3329=ORIENTED_EDGE('',*,*,#2280,.F.);
#3330=ORIENTED_EDGE('',*,*,#2281,.T.);
#3331=ORIENTED_EDGE('',*,*,#2280,.T.);
#3332=ORIENTED_EDGE('',*,*,#2282,.F.);
#3333=ORIENTED_EDGE('',*,*,#2283,.F.);
#3334=ORIENTED_EDGE('',*,*,#2284,.T.);
#3335=ORIENTED_EDGE('',*,*,#2283,.T.);
#3336=ORIENTED_EDGE('',*,*,#2285,.F.);
#3337=ORIENTED_EDGE('',*,*,#2275,.F.);
#3338=ORIENTED_EDGE('',*,*,#2286,.T.);
#3339=ORIENTED_EDGE('',*,*,#2287,.T.);
#3340=ORIENTED_EDGE('',*,*,#2288,.F.);
#3341=ORIENTED_EDGE('',*,*,#2289,.F.);
#3342=ORIENTED_EDGE('',*,*,#2290,.T.);
#3343=ORIENTED_EDGE('',*,*,#2289,.T.);
#3344=ORIENTED_EDGE('',*,*,#2291,.F.);
#3345=ORIENTED_EDGE('',*,*,#2292,.F.);
#3346=ORIENTED_EDGE('',*,*,#2293,.T.);
#3347=ORIENTED_EDGE('',*,*,#2292,.T.);
#3348=ORIENTED_EDGE('',*,*,#2294,.F.);
#3349=ORIENTED_EDGE('',*,*,#2295,.F.);
#3350=ORIENTED_EDGE('',*,*,#2296,.T.);
#3351=ORIENTED_EDGE('',*,*,#2295,.T.);
#3352=ORIENTED_EDGE('',*,*,#2297,.F.);
#3353=ORIENTED_EDGE('',*,*,#2298,.F.);
#3354=ORIENTED_EDGE('',*,*,#2299,.T.);
#3355=ORIENTED_EDGE('',*,*,#2298,.T.);
#3356=ORIENTED_EDGE('',*,*,#2300,.F.);
#3357=ORIENTED_EDGE('',*,*,#2301,.F.);
#3358=ORIENTED_EDGE('',*,*,#2302,.T.);
#3359=ORIENTED_EDGE('',*,*,#2301,.T.);
#3360=ORIENTED_EDGE('',*,*,#2303,.F.);
#3361=ORIENTED_EDGE('',*,*,#2287,.F.);
#3362=ORIENTED_EDGE('',*,*,#2303,.T.);
#3363=ORIENTED_EDGE('',*,*,#2300,.T.);
#3364=ORIENTED_EDGE('',*,*,#2297,.T.);
#3365=ORIENTED_EDGE('',*,*,#2294,.T.);
#3366=ORIENTED_EDGE('',*,*,#2291,.T.);
#3367=ORIENTED_EDGE('',*,*,#2288,.T.);
#3368=ORIENTED_EDGE('',*,*,#2285,.T.);
#3369=ORIENTED_EDGE('',*,*,#2282,.T.);
#3370=ORIENTED_EDGE('',*,*,#2279,.T.);
#3371=ORIENTED_EDGE('',*,*,#2276,.T.);
#3372=ORIENTED_EDGE('',*,*,#2302,.F.);
#3373=ORIENTED_EDGE('',*,*,#2286,.F.);
#3374=ORIENTED_EDGE('',*,*,#2290,.F.);
#3375=ORIENTED_EDGE('',*,*,#2293,.F.);
#3376=ORIENTED_EDGE('',*,*,#2296,.F.);
#3377=ORIENTED_EDGE('',*,*,#2299,.F.);
#3378=ORIENTED_EDGE('',*,*,#2284,.F.);
#3379=ORIENTED_EDGE('',*,*,#2274,.F.);
#3380=ORIENTED_EDGE('',*,*,#2278,.F.);
#3381=ORIENTED_EDGE('',*,*,#2281,.F.);
#3469=CYLINDRICAL_SURFACE('',#4087,4.433);
#3470=CYLINDRICAL_SURFACE('',#4090,3.72275);
#3661=ADVANCED_FACE('',(#569),#94,.T.);
#3662=ADVANCED_FACE('',(#570),#3469,.F.);
#3663=ADVANCED_FACE('',(#571),#95,.T.);
#3664=ADVANCED_FACE('',(#572),#3470,.F.);
#3665=ADVANCED_FACE('',(#573),#246,.T.);
#3666=ADVANCED_FACE('',(#574),#247,.T.);
#3667=ADVANCED_FACE('',(#575),#248,.T.);
#3668=ADVANCED_FACE('',(#576),#249,.T.);
#3669=ADVANCED_FACE('',(#577),#250,.T.);
#3670=ADVANCED_FACE('',(#578),#251,.T.);
#3671=ADVANCED_FACE('',(#579,#201),#252,.T.);
#3672=ADVANCED_FACE('',(#580,#202),#253,.F.);
#3687=CLOSED_SHELL('',(#3661,#3662,#3663,#3664,#3665,#3666,#3667,#3668,
#3669,#3670,#3671,#3672));
#4086=AXIS2_PLACEMENT_3D('',#25706,#4822,#4823);
#4087=AXIS2_PLACEMENT_3D('',#25769,#4826,#4827);
#4088=AXIS2_PLACEMENT_3D('',#25771,#4828,#4829);
#4089=AXIS2_PLACEMENT_3D('',#25773,#4830,#4831);
#4090=AXIS2_PLACEMENT_3D('',#25834,#4834,#4835);
#4091=AXIS2_PLACEMENT_3D('',#25835,#4836,#4837);
#4092=AXIS2_PLACEMENT_3D('',#25836,#4838,#4839);
#4093=AXIS2_PLACEMENT_3D('',#25837,#4840,#4841);
#4094=AXIS2_PLACEMENT_3D('',#25846,#4846,#4847);
#4095=AXIS2_PLACEMENT_3D('',#25852,#4851,#4852);
#4096=AXIS2_PLACEMENT_3D('',#25858,#4856,#4857);
#4097=AXIS2_PLACEMENT_3D('',#25864,#4861,#4862);
#4098=AXIS2_PLACEMENT_3D('',#25870,#4866,#4867);
#4099=AXIS2_PLACEMENT_3D('',#25873,#4870,#4871);
#4100=AXIS2_PLACEMENT_3D('',#25874,#4872,#4873);
#4822=DIRECTION('axis',(0.,0.,1.));
#4823=DIRECTION('refdir',(1.,0.,0.));
#4824=DIRECTION('',(1.,0.,0.));
#4825=DIRECTION('',(1.,0.,0.));
#4826=DIRECTION('center_axis',(1.,0.,0.));
#4827=DIRECTION('ref_axis',(0.,0.444750988585694,0.895654262621492));
#4828=DIRECTION('center_axis',(-1.,0.,0.));
#4829=DIRECTION('ref_axis',(0.,0.444750988585694,0.895654262621492));
#4830=DIRECTION('center_axis',(-1.,0.,0.));
#4831=DIRECTION('ref_axis',(0.,0.444750988585694,0.895654262621492));
#4832=DIRECTION('',(1.,0.,0.));
#4833=DIRECTION('',(1.,0.,0.));
#4834=DIRECTION('center_axis',(1.,0.,0.));
#4835=DIRECTION('ref_axis',(0.,-0.580623944517215,-0.814171870708679));
#4836=DIRECTION('center_axis',(-1.,0.,0.));
#4837=DIRECTION('ref_axis',(0.,-0.580623944517215,-0.814171870708679));
#4838=DIRECTION('center_axis',(-1.,0.,0.));
#4839=DIRECTION('ref_axis',(0.,-0.580623944517215,-0.814171870708679));
#4840=DIRECTION('center_axis',(0.,0.866025403784439,0.5));
#4841=DIRECTION('ref_axis',(0.,-0.5,0.866025403784439));
#4842=DIRECTION('',(0.,-0.5,0.866025403784439));
#4843=DIRECTION('',(1.,0.,0.));
#4844=DIRECTION('',(0.,-0.5,0.866025403784439));
#4845=DIRECTION('',(1.,0.,0.));
#4846=DIRECTION('center_axis',(0.,0.866025403784438,-0.5));
#4847=DIRECTION('ref_axis',(0.,0.5,0.866025403784438));
#4848=DIRECTION('',(0.,0.5,0.866025403784438));
#4849=DIRECTION('',(0.,0.5,0.866025403784438));
#4850=DIRECTION('',(1.,0.,0.));
#4851=DIRECTION('center_axis',(0.,-3.02823770847138E-16,-1.));
#4852=DIRECTION('ref_axis',(0.,1.,-3.02823770847138E-16));
#4853=DIRECTION('',(0.,1.,-3.02823770847138E-16));
#4854=DIRECTION('',(0.,1.,-3.02823770847138E-16));
#4855=DIRECTION('',(1.,0.,0.));
#4856=DIRECTION('center_axis',(0.,-0.866025403784439,-0.5));
#4857=DIRECTION('ref_axis',(0.,0.5,-0.866025403784439));
#4858=DIRECTION('',(0.,0.5,-0.866025403784439));
#4859=DIRECTION('',(0.,0.5,-0.866025403784439));
#4860=DIRECTION('',(1.,0.,0.));
#4861=DIRECTION('center_axis',(0.,-0.866025403784439,0.5));
#4862=DIRECTION('ref_axis',(0.,-0.5,-0.866025403784439));
#4863=DIRECTION('',(0.,-0.5,-0.866025403784439));
#4864=DIRECTION('',(0.,-0.5,-0.866025403784439));
#4865=DIRECTION('',(1.,0.,0.));
#4866=DIRECTION('center_axis',(0.,6.05647541694275E-16,1.));
#4867=DIRECTION('ref_axis',(0.,-1.,6.05647541694275E-16));
#4868=DIRECTION('',(0.,-1.,6.05647541694275E-16));
#4869=DIRECTION('',(0.,-1.,6.05647541694275E-16));
#4870=DIRECTION('center_axis',(1.,0.,0.));
#4871=DIRECTION('ref_axis',(0.,1.,0.));
#4872=DIRECTION('center_axis',(1.,0.,0.));
#4873=DIRECTION('ref_axis',(0.,1.,0.));
#25706=CARTESIAN_POINT('',(0.,0.,0.));
#25707=CARTESIAN_POINT('Ctrl Pts',(82.4430005297901,1.97158113240038,3.97043534620108));
#25708=CARTESIAN_POINT('Ctrl Pts',(87.2430005297901,1.97158113240038,3.97043534620108));
#25709=CARTESIAN_POINT('Ctrl Pts',(82.4430005297901,2.29671111436096,3.77621792657108));
#25710=CARTESIAN_POINT('Ctrl Pts',(87.2430005297901,2.29671111436096,3.77621792657108));
#25711=CARTESIAN_POINT('Ctrl Pts',(82.4430005297901,2.59552275281558,3.54102114079632));
#25712=CARTESIAN_POINT('Ctrl Pts',(87.2430005297901,2.59552275281558,3.54102114079632));
#25713=CARTESIAN_POINT('Ctrl Pts',(82.4430005297901,3.11908576775695,3.00435277140383));
#25714=CARTESIAN_POINT('Ctrl Pts',(87.2430005297901,3.11908576775695,3.00435277140383));
#25715=CARTESIAN_POINT('Ctrl Pts',(82.4430005297901,3.34301024132503,2.70651491388494));
#25716=CARTESIAN_POINT('Ctrl Pts',(87.2430005297901,3.34301024132503,2.70651491388494));
#25717=CARTESIAN_POINT('Ctrl Pts',(82.4430005297901,3.79251211736076,1.90981794028965));
#25718=CARTESIAN_POINT('Ctrl Pts',(87.2430005297901,3.79251211736076,1.90981794028965));
#25719=CARTESIAN_POINT('Ctrl Pts',(82.4430005297901,3.96610878107774,1.3893796287376));
#25720=CARTESIAN_POINT('Ctrl Pts',(87.2430005297901,3.96610878107774,1.3893796287376));
#25721=CARTESIAN_POINT('Ctrl Pts',(82.4430005297901,4.09877879619631,0.327978495265378));
#25722=CARTESIAN_POINT('Ctrl Pts',(87.2430005297901,4.09877879619631,0.327978495265378));
#25723=CARTESIAN_POINT('Ctrl Pts',(82.4430005297901,4.06307606785725,-0.201870082003989));
#25724=CARTESIAN_POINT('Ctrl Pts',(87.2430005297901,4.06307606785725,-0.201870082003989));
#25725=CARTESIAN_POINT('Ctrl Pts',(82.4430005297901,3.79206680758235,-1.20058842967181));
#25726=CARTESIAN_POINT('Ctrl Pts',(87.2430005297901,3.79206680758235,-1.20058842967181));
#25727=CARTESIAN_POINT('Ctrl Pts',(82.4430005297901,3.56572122172907,-1.66148594501202));
#25728=CARTESIAN_POINT('Ctrl Pts',(87.2430005297901,3.56572122172907,-1.66148594501202));
#25729=CARTESIAN_POINT('Ctrl Pts',(82.4430005297901,2.95711124459234,-2.45497912282895));
#25730=CARTESIAN_POINT('Ctrl Pts',(87.2430005297901,2.95711124459234,-2.45497912282895));
#25731=CARTESIAN_POINT('Ctrl Pts',(82.4430005297901,2.58595465431404,-2.78386901588456));
#25732=CARTESIAN_POINT('Ctrl Pts',(87.2430005297901,2.58595465431404,-2.78386901588456));
#25733=CARTESIAN_POINT('Ctrl Pts',(82.4430005297901,2.16151778945147,-3.03095833168073));
#25734=CARTESIAN_POINT('Ctrl Pts',(87.2430005297901,2.16151778945147,-3.03095833168073));
#25735=CARTESIAN_POINT('',(82.4430005297901,1.97158113240038,3.97043534620107));
#25736=CARTESIAN_POINT('',(82.4430005297901,2.16151778945147,-3.03095833168073));
#25737=CARTESIAN_POINT('Ctrl Pts',(82.4430005297901,1.97158113240038,3.97043534620108));
#25738=CARTESIAN_POINT('Ctrl Pts',(82.4430005297901,2.29671111436096,3.77621792657108));
#25739=CARTESIAN_POINT('Ctrl Pts',(82.4430005297901,2.59552275281558,3.54102114079632));
#25740=CARTESIAN_POINT('Ctrl Pts',(82.4430005297901,3.11908576775695,3.00435277140383));
#25741=CARTESIAN_POINT('Ctrl Pts',(82.4430005297901,3.34301024132503,2.70651491388494));
#25742=CARTESIAN_POINT('Ctrl Pts',(82.4430005297901,3.79251211736076,1.90981794028965));
#25743=CARTESIAN_POINT('Ctrl Pts',(82.4430005297901,3.96610878107774,1.3893796287376));
#25744=CARTESIAN_POINT('Ctrl Pts',(82.4430005297901,4.09877879619631,0.327978495265378));
#25745=CARTESIAN_POINT('Ctrl Pts',(82.4430005297901,4.06307606785725,-0.201870082003989));
#25746=CARTESIAN_POINT('Ctrl Pts',(82.4430005297901,3.79206680758235,-1.20058842967181));
#25747=CARTESIAN_POINT('Ctrl Pts',(82.4430005297901,3.56572122172907,-1.66148594501202));
#25748=CARTESIAN_POINT('Ctrl Pts',(82.4430005297901,2.95711124459234,-2.45497912282895));
#25749=CARTESIAN_POINT('Ctrl Pts',(82.4430005297901,2.58595465431404,-2.78386901588456));
#25750=CARTESIAN_POINT('Ctrl Pts',(82.4430005297901,2.16151778945147,-3.03095833168073));
#25751=CARTESIAN_POINT('',(86.4430005297901,2.16151778945147,-3.03095833168073));
#25752=CARTESIAN_POINT('',(82.4430005297901,2.16151778945147,-3.03095833168073));
#25753=CARTESIAN_POINT('',(86.4430005297901,1.97158113240038,3.97043534620107));
#25754=CARTESIAN_POINT('Ctrl Pts',(86.4430005297901,1.97158113240038,3.97043534620108));
#25755=CARTESIAN_POINT('Ctrl Pts',(86.4430005297901,2.29671111436096,3.77621792657108));
#25756=CARTESIAN_POINT('Ctrl Pts',(86.4430005297901,2.59552275281558,3.54102114079632));
#25757=CARTESIAN_POINT('Ctrl Pts',(86.4430005297901,3.11908576775695,3.00435277140383));
#25758=CARTESIAN_POINT('Ctrl Pts',(86.4430005297901,3.34301024132503,2.70651491388494));
#25759=CARTESIAN_POINT('Ctrl Pts',(86.4430005297901,3.79251211736076,1.90981794028965));
#25760=CARTESIAN_POINT('Ctrl Pts',(86.4430005297901,3.96610878107774,1.3893796287376));
#25761=CARTESIAN_POINT('Ctrl Pts',(86.4430005297901,4.09877879619631,0.327978495265378));
#25762=CARTESIAN_POINT('Ctrl Pts',(86.4430005297901,4.06307606785725,-0.201870082003989));
#25763=CARTESIAN_POINT('Ctrl Pts',(86.4430005297901,3.79206680758235,-1.20058842967181));
#25764=CARTESIAN_POINT('Ctrl Pts',(86.4430005297901,3.56572122172907,-1.66148594501202));
#25765=CARTESIAN_POINT('Ctrl Pts',(86.4430005297901,2.95711124459234,-2.45497912282895));
#25766=CARTESIAN_POINT('Ctrl Pts',(86.4430005297901,2.58595465431404,-2.78386901588456));
#25767=CARTESIAN_POINT('Ctrl Pts',(86.4430005297901,2.16151778945147,-3.03095833168073));
#25768=CARTESIAN_POINT('',(82.4430005297901,1.97158113240038,3.97043534620107));
#25769=CARTESIAN_POINT('Origin',(82.4430005297901,-2.77555756156289E-16,
5.55111512312578E-16));
#25770=CARTESIAN_POINT('',(82.4430005297901,-1.97158113240039,3.97043534620107));
#25771=CARTESIAN_POINT('Origin',(82.4430005297901,-2.77555756156289E-16,
5.55111512312578E-16));
#25772=CARTESIAN_POINT('',(86.4430005297901,-1.97158113240039,3.97043534620107));
#25773=CARTESIAN_POINT('Origin',(86.4430005297901,-2.77555756156289E-16,
5.55111512312578E-16));
#25774=CARTESIAN_POINT('',(82.4430005297901,-1.97158113240039,3.97043534620107));
#25775=CARTESIAN_POINT('Ctrl Pts',(82.4430005297901,-2.16151778945139,-3.03095833168078));
#25776=CARTESIAN_POINT('Ctrl Pts',(87.2430005297901,-2.16151778945139,-3.03095833168078));
#25777=CARTESIAN_POINT('Ctrl Pts',(82.4430005297901,-2.4417969811413,-2.86779155838698));
#25778=CARTESIAN_POINT('Ctrl Pts',(87.2430005297901,-2.4417969811413,-2.86779155838698));
#25779=CARTESIAN_POINT('Ctrl Pts',(82.4430005297901,-2.69946597133354,-2.66855779259647));
#25780=CARTESIAN_POINT('Ctrl Pts',(87.2430005297901,-2.69946597133354,-2.66855779259647));
#25781=CARTESIAN_POINT('Ctrl Pts',(82.4430005297901,-3.16313807023027,-2.20413689736136));
#25782=CARTESIAN_POINT('Ctrl Pts',(87.2430005297901,-3.16313807023027,-2.20413689736136));
#25783=CARTESIAN_POINT('Ctrl Pts',(82.4430005297901,-3.36582061002206,-1.93954623621156));
#25784=CARTESIAN_POINT('Ctrl Pts',(87.2430005297901,-3.36582061002206,-1.93954623621156));
#25785=CARTESIAN_POINT('Ctrl Pts',(82.4430005297901,-3.7905877946382,-1.20735040930033));
#25786=CARTESIAN_POINT('Ctrl Pts',(87.2430005297901,-3.7905877946382,-1.20735040930033));
#25787=CARTESIAN_POINT('Ctrl Pts',(82.4430005297901,-3.95787261855977,-0.715467908482556));
#25788=CARTESIAN_POINT('Ctrl Pts',(87.2430005297901,-3.95787261855977,-0.715467908482556));
#25789=CARTESIAN_POINT('Ctrl Pts',(82.4430005297901,-4.0999785741866,0.321696095215354));
#25790=CARTESIAN_POINT('Ctrl Pts',(87.2430005297901,-4.0999785741866,0.321696095215354));
#25791=CARTESIAN_POINT('Ctrl Pts',(82.4430005297901,-4.06691955087291,0.857794436836504));
#25792=CARTESIAN_POINT('Ctrl Pts',(87.2430005297901,-4.06691955087291,0.857794436836504));
#25793=CARTESIAN_POINT('Ctrl Pts',(82.4430005297901,-3.79581350913489,1.90493582172488));
#25794=CARTESIAN_POINT('Ctrl Pts',(87.2430005297901,-3.79581350913489,1.90493582172488));
#25795=CARTESIAN_POINT('Ctrl Pts',(82.4430005297901,-3.55404702294629,2.40416273654669));
#25796=CARTESIAN_POINT('Ctrl Pts',(87.2430005297901,-3.55404702294629,2.40416273654669));
#25797=CARTESIAN_POINT('Ctrl Pts',(82.4430005297901,-2.88474862400959,3.29779955123577));
#25798=CARTESIAN_POINT('Ctrl Pts',(87.2430005297901,-2.88474862400959,3.29779955123577));
#25799=CARTESIAN_POINT('Ctrl Pts',(82.4430005297901,-2.45846445810197,3.67959405679301));
#25800=CARTESIAN_POINT('Ctrl Pts',(87.2430005297901,-2.45846445810197,3.67959405679301));
#25801=CARTESIAN_POINT('Ctrl Pts',(82.4430005297901,-1.97158113240039,3.97043534620107));
#25802=CARTESIAN_POINT('Ctrl Pts',(87.2430005297901,-1.97158113240039,3.97043534620107));
#25803=CARTESIAN_POINT('',(82.4430005297901,-2.16151778945139,-3.03095833168078));
#25804=CARTESIAN_POINT('Ctrl Pts',(82.4430005297901,-2.16151778945139,-3.03095833168078));
#25805=CARTESIAN_POINT('Ctrl Pts',(82.4430005297901,-2.4417969811413,-2.86779155838698));
#25806=CARTESIAN_POINT('Ctrl Pts',(82.4430005297901,-2.69946597133354,-2.66855779259647));
#25807=CARTESIAN_POINT('Ctrl Pts',(82.4430005297901,-3.16313807023027,-2.20413689736136));
#25808=CARTESIAN_POINT('Ctrl Pts',(82.4430005297901,-3.36582061002206,-1.93954623621156));
#25809=CARTESIAN_POINT('Ctrl Pts',(82.4430005297901,-3.7905877946382,-1.20735040930033));
#25810=CARTESIAN_POINT('Ctrl Pts',(82.4430005297901,-3.95787261855977,-0.715467908482556));
#25811=CARTESIAN_POINT('Ctrl Pts',(82.4430005297901,-4.0999785741866,0.321696095215354));
#25812=CARTESIAN_POINT('Ctrl Pts',(82.4430005297901,-4.06691955087291,0.857794436836504));
#25813=CARTESIAN_POINT('Ctrl Pts',(82.4430005297901,-3.79581350913489,1.90493582172488));
#25814=CARTESIAN_POINT('Ctrl Pts',(82.4430005297901,-3.55404702294629,2.40416273654669));
#25815=CARTESIAN_POINT('Ctrl Pts',(82.4430005297901,-2.88474862400959,3.29779955123577));
#25816=CARTESIAN_POINT('Ctrl Pts',(82.4430005297901,-2.45846445810197,3.67959405679301));
#25817=CARTESIAN_POINT('Ctrl Pts',(82.4430005297901,-1.97158113240039,3.97043534620107));
#25818=CARTESIAN_POINT('',(86.4430005297901,-2.16151778945139,-3.03095833168078));
#25819=CARTESIAN_POINT('Ctrl Pts',(86.4430005297901,-2.16151778945139,-3.03095833168078));
#25820=CARTESIAN_POINT('Ctrl Pts',(86.4430005297901,-2.4417969811413,-2.86779155838698));
#25821=CARTESIAN_POINT('Ctrl Pts',(86.4430005297901,-2.69946597133354,-2.66855779259647));
#25822=CARTESIAN_POINT('Ctrl Pts',(86.4430005297901,-3.16313807023027,-2.20413689736136));
#25823=CARTESIAN_POINT('Ctrl Pts',(86.4430005297901,-3.36582061002206,-1.93954623621156));
#25824=CARTESIAN_POINT('Ctrl Pts',(86.4430005297901,-3.7905877946382,-1.20735040930033));
#25825=CARTESIAN_POINT('Ctrl Pts',(86.4430005297901,-3.95787261855977,-0.715467908482556));
#25826=CARTESIAN_POINT('Ctrl Pts',(86.4430005297901,-4.0999785741866,0.321696095215354));
#25827=CARTESIAN_POINT('Ctrl Pts',(86.4430005297901,-4.06691955087291,0.857794436836504));
#25828=CARTESIAN_POINT('Ctrl Pts',(86.4430005297901,-3.79581350913489,1.90493582172488));
#25829=CARTESIAN_POINT('Ctrl Pts',(86.4430005297901,-3.55404702294629,2.40416273654669));
#25830=CARTESIAN_POINT('Ctrl Pts',(86.4430005297901,-2.88474862400959,3.29779955123577));
#25831=CARTESIAN_POINT('Ctrl Pts',(86.4430005297901,-2.45846445810197,3.67959405679301));
#25832=CARTESIAN_POINT('Ctrl Pts',(86.4430005297901,-1.97158113240039,3.97043534620107));
#25833=CARTESIAN_POINT('',(82.4430005297901,-2.16151778945139,-3.03095833168078));
#25834=CARTESIAN_POINT('Origin',(82.4430005297901,-2.77555756156289E-16,
5.55111512312578E-16));
#25835=CARTESIAN_POINT('Origin',(82.4430005297901,-2.77555756156289E-16,
5.55111512312578E-16));
#25836=CARTESIAN_POINT('Origin',(86.4430005297901,-2.77555756156289E-16,
5.55111512312578E-16));
#25837=CARTESIAN_POINT('Origin',(82.4430005297901,7.33246945257534,-3.33066907387547E-15));
#25838=CARTESIAN_POINT('',(82.4430005297901,7.33246945257534,-3.33066907387547E-15));
#25839=CARTESIAN_POINT('',(82.4430005297901,3.66623472628768,6.35010481840362));
#25840=CARTESIAN_POINT('',(82.4430005297901,7.33246945257534,-3.33066907387547E-15));
#25841=CARTESIAN_POINT('',(86.4430005297901,3.66623472628768,6.35010481840362));
#25842=CARTESIAN_POINT('',(82.4430005297901,3.66623472628768,6.35010481840362));
#25843=CARTESIAN_POINT('',(86.4430005297901,7.33246945257534,-3.33066907387547E-15));
#25844=CARTESIAN_POINT('',(86.4430005297901,7.33246945257534,-3.33066907387547E-15));
#25845=CARTESIAN_POINT('',(82.4430005297901,7.33246945257534,-3.33066907387547E-15));
#25846=CARTESIAN_POINT('Origin',(82.4430005297901,3.66623472628767,-6.35010481840363));
#25847=CARTESIAN_POINT('',(82.4430005297901,3.66623472628767,-6.35010481840363));
#25848=CARTESIAN_POINT('',(82.4430005297901,3.66623472628767,-6.35010481840363));
#25849=CARTESIAN_POINT('',(86.4430005297901,3.66623472628767,-6.35010481840363));
#25850=CARTESIAN_POINT('',(86.4430005297901,3.66623472628767,-6.35010481840363));
#25851=CARTESIAN_POINT('',(82.4430005297901,3.66623472628767,-6.35010481840363));
#25852=CARTESIAN_POINT('Origin',(82.4430005297901,-3.66623472628767,-6.35010481840362));
#25853=CARTESIAN_POINT('',(82.4430005297901,-3.66623472628767,-6.35010481840362));
#25854=CARTESIAN_POINT('',(82.4430005297901,-3.66623472628767,-6.35010481840362));
#25855=CARTESIAN_POINT('',(86.4430005297901,-3.66623472628767,-6.35010481840362));
#25856=CARTESIAN_POINT('',(86.4430005297901,-3.66623472628767,-6.35010481840362));
#25857=CARTESIAN_POINT('',(82.4430005297901,-3.66623472628767,-6.35010481840362));
#25858=CARTESIAN_POINT('Origin',(82.4430005297901,-7.33246945257535,2.77555756156289E-15));
#25859=CARTESIAN_POINT('',(82.4430005297901,-7.33246945257535,2.77555756156289E-15));
#25860=CARTESIAN_POINT('',(82.4430005297901,-7.33246945257535,2.77555756156289E-15));
#25861=CARTESIAN_POINT('',(86.4430005297901,-7.33246945257535,2.77555756156289E-15));
#25862=CARTESIAN_POINT('',(86.4430005297901,-7.33246945257535,2.77555756156289E-15));
#25863=CARTESIAN_POINT('',(82.4430005297901,-7.33246945257535,2.77555756156289E-15));
#25864=CARTESIAN_POINT('Origin',(82.4430005297901,-3.66623472628767,6.35010481840363));
#25865=CARTESIAN_POINT('',(82.4430005297901,-3.66623472628767,6.35010481840363));
#25866=CARTESIAN_POINT('',(82.4430005297901,-3.66623472628767,6.35010481840363));
#25867=CARTESIAN_POINT('',(86.4430005297901,-3.66623472628767,6.35010481840363));
#25868=CARTESIAN_POINT('',(86.4430005297901,-3.66623472628767,6.35010481840363));
#25869=CARTESIAN_POINT('',(82.4430005297901,-3.66623472628767,6.35010481840363));
#25870=CARTESIAN_POINT('Origin',(82.4430005297901,3.66623472628768,6.35010481840362));
#25871=CARTESIAN_POINT('',(82.4430005297901,3.66623472628768,6.35010481840362));
#25872=CARTESIAN_POINT('',(86.4430005297901,3.66623472628768,6.35010481840362));
#25873=CARTESIAN_POINT('Origin',(86.4430005297901,0.,0.));
#25874=CARTESIAN_POINT('Origin',(82.4430005297901,0.,0.));
#28041=UNCERTAINTY_MEASURE_WITH_UNIT(LENGTH_MEASURE(0.01),#28056,
'DISTANCE_ACCURACY_VALUE',
'Maximum model space distance between geometric entities at asserted c
onnectivities');
#28043=UNCERTAINTY_MEASURE_WITH_UNIT(LENGTH_MEASURE(0.01),#28056,
'DISTANCE_ACCURACY_VALUE',
'Maximum model space distance between geometric entities at asserted c
onnectivities');
#28053=(
GEOMETRIC_REPRESENTATION_CONTEXT(3)
GLOBAL_UNCERTAINTY_ASSIGNED_CONTEXT((#28041))
GLOBAL_UNIT_ASSIGNED_CONTEXT((#28056,#28058,#28059))
REPRESENTATION_CONTEXT('','3D')
);
#28055=(
GEOMETRIC_REPRESENTATION_CONTEXT(3)
GLOBAL_UNCERTAINTY_ASSIGNED_CONTEXT((#28043))
GLOBAL_UNIT_ASSIGNED_CONTEXT((#28056,#28058,#28059))
REPRESENTATION_CONTEXT('','3D')
);
#28056=(
LENGTH_UNIT()
NAMED_UNIT(*)
SI_UNIT(.MILLI.,.METRE.)
);
#28058=(
NAMED_UNIT(*)
PLANE_ANGLE_UNIT()
SI_UNIT($,.RADIAN.)
);
#28059=(
NAMED_UNIT(*)
SI_UNIT($,.STERADIAN.)
SOLID_ANGLE_UNIT()
);
#28069=SHAPE_DEFINITION_REPRESENTATION(#28080,#28101);
#28080=PRODUCT_DEFINITION_SHAPE('',$,#28113);
#28101=SHAPE_REPRESENTATION('',(#4086),#28053);
#28103=PRODUCT_DEFINITION_CONTEXT('part definition',#28138,'design');
#28113=PRODUCT_DEFINITION('Nut_01','Nut_01',#28124,#28103);
#28124=PRODUCT_DEFINITION_FORMATION('',$,#28149);
#28138=APPLICATION_CONTEXT(
'Core Data for Automotive Mechanical Design Process');
#28139=PRODUCT_CONTEXT('part definition',#28138,'mechanical');
#28149=PRODUCT('Nut_01','Nut_01',$,(#28139));
#28152=PRESENTATION_STYLE_ASSIGNMENT((#28155));
#28155=SURFACE_STYLE_USAGE(.BOTH.,#28158);
#28158=SURFACE_SIDE_STYLE('',(#28161));
#28161=SURFACE_STYLE_FILL_AREA(#28164);
#28164=FILL_AREA_STYLE('Opaque(160,160,160)',(#28167));
#28167=FILL_AREA_STYLE_COLOUR('Opaque(160,160,160)',#28170);
#28170=COLOUR_RGB('Opaque(160,160,160)', 0.66274510, 0.83137255, 0.94901961);
ENDSEC;
END-ISO-10303-21;
